ISO-10303-21;
HEADER;
/* Generated by software containing ST-Developer
 * from STEP Tools, Inc. (www.steptools.com) 
 */

FILE_DESCRIPTION(
/* description */ ('Bell-crank linkage with push rods'),
/* implementation_level */ '2;1');

FILE_NAME(
/* name */ 'Plain link bushing (2).step',
/* time_stamp */ '2026-10-28T03:25:15-07:00',
/* author */ (''),
/* organization */ (''),
/* preprocessor_version */ 'ST-DEVELOPER v20.2',
/* originating_system */ 'Autodesk Translation Framework v15.17.0.0',
/* authorisation */ '');

FILE_SCHEMA (('AUTOMOTIVE_DESIGN { 1 0 10303 214 3 1 1 }'));
ENDSEC;

DATA;
#10=MECHANICAL_DESIGN_GEOMETRIC_PRESENTATION_REPRESENTATION('',(#647),#16678);
#531=SHAPE_REPRESENTATION_RELATIONSHIP('SRR','None',#16951,#585);
#585=ADVANCED_BREP_SHAPE_REPRESENTATION('',(#707),#16656);
#647=STYLED_ITEM('',(#17284),#707);
#707=MANIFOLD_SOLID_BREP('Body1',#8839);
#870=FACE_BOUND('',#2278,.T.);
#871=FACE_BOUND('',#2280,.T.);
#1155=PLANE('',#10220);
#1156=PLANE('',#10221);
#1608=FACE_OUTER_BOUND('',#2275,.T.);
#1609=FACE_OUTER_BOUND('',#2276,.T.);
#1610=FACE_OUTER_BOUND('',#2277,.T.);
#1611=FACE_OUTER_BOUND('',#2279,.T.);
#2275=EDGE_LOOP('',(#7431,#7432,#7433,#7434));
#2276=EDGE_LOOP('',(#7435,#7436,#7437,#7438));
#2277=EDGE_LOOP('',(#7439));
#2278=EDGE_LOOP('',(#7440));
#2279=EDGE_LOOP('',(#7441));
#2280=EDGE_LOOP('',(#7442));
#2904=LINE('',#15751,#3453);
#2905=LINE('',#15757,#3454);
#3453=VECTOR('',#12526,0.305);
#3454=VECTOR('',#12533,0.5);
#3979=CIRCLE('',#10215,0.305);
#3980=CIRCLE('',#10216,0.305);
#3981=CIRCLE('',#10218,0.5);
#3982=CIRCLE('',#10219,0.5);
#4622=VERTEX_POINT('',#15748);
#4623=VERTEX_POINT('',#15750);
#4624=VERTEX_POINT('',#15754);
#4625=VERTEX_POINT('',#15756);
#5593=EDGE_CURVE('',#4622,#4622,#3979,.T.);
#5594=EDGE_CURVE('',#4622,#4623,#2904,.T.);
#5595=EDGE_CURVE('',#4623,#4623,#3980,.T.);
#5596=EDGE_CURVE('',#4624,#4624,#3981,.T.);
#5597=EDGE_CURVE('',#4624,#4625,#2905,.T.);
#5598=EDGE_CURVE('',#4625,#4625,#3982,.T.);
#7431=ORIENTED_EDGE('',*,*,#5593,.F.);
#7432=ORIENTED_EDGE('',*,*,#5594,.T.);
#7433=ORIENTED_EDGE('',*,*,#5595,.T.);
#7434=ORIENTED_EDGE('',*,*,#5594,.F.);
#7435=ORIENTED_EDGE('',*,*,#5596,.F.);
#7436=ORIENTED_EDGE('',*,*,#5597,.T.);
#7437=ORIENTED_EDGE('',*,*,#5598,.T.);
#7438=ORIENTED_EDGE('',*,*,#5597,.F.);
#7439=ORIENTED_EDGE('',*,*,#5596,.T.);
#7440=ORIENTED_EDGE('',*,*,#5593,.T.);
#7441=ORIENTED_EDGE('',*,*,#5598,.F.);
#7442=ORIENTED_EDGE('',*,*,#5595,.F.);
#8206=CYLINDRICAL_SURFACE('',#10214,0.305);
#8207=CYLINDRICAL_SURFACE('',#10217,0.5);
#8633=ADVANCED_FACE('',(#1608),#8206,.F.);
#8634=ADVANCED_FACE('',(#1609),#8207,.T.);
#8635=ADVANCED_FACE('',(#1610,#870),#1155,.T.);
#8636=ADVANCED_FACE('',(#1611,#871),#1156,.F.);
#8839=CLOSED_SHELL('',(#8633,#8634,#8635,#8636));
#10213=AXIS2_PLACEMENT_3D('',#15746,#12520,#12521);
#10214=AXIS2_PLACEMENT_3D('',#15747,#12522,#12523);
#10215=AXIS2_PLACEMENT_3D('',#15749,#12524,#12525);
#10216=AXIS2_PLACEMENT_3D('',#15752,#12527,#12528);
#10217=AXIS2_PLACEMENT_3D('',#15753,#12529,#12530);
#10218=AXIS2_PLACEMENT_3D('',#15755,#12531,#12532);
#10219=AXIS2_PLACEMENT_3D('',#15758,#12534,#12535);
#10220=AXIS2_PLACEMENT_3D('',#15759,#12536,#12537);
#10221=AXIS2_PLACEMENT_3D('',#15760,#12538,#12539);
#12520=DIRECTION('axis',(0.,0.,1.));
#12521=DIRECTION('refdir',(1.,0.,0.));
#12522=DIRECTION('center_axis',(0.,0.,1.));
#12523=DIRECTION('ref_axis',(1.,0.,0.));
#12524=DIRECTION('center_axis',(0.,0.,-1.));
#12525=DIRECTION('ref_axis',(1.,0.,0.));
#12526=DIRECTION('',(0.,0.,-1.));
#12527=DIRECTION('center_axis',(0.,0.,-1.));
#12528=DIRECTION('ref_axis',(1.,0.,0.));
#12529=DIRECTION('center_axis',(0.,0.,1.));
#12530=DIRECTION('ref_axis',(1.,0.,0.));
#12531=DIRECTION('center_axis',(0.,0.,1.));
#12532=DIRECTION('ref_axis',(1.,0.,0.));
#12533=DIRECTION('',(0.,0.,-1.));
#12534=DIRECTION('center_axis',(0.,0.,1.));
#12535=DIRECTION('ref_axis',(1.,0.,0.));
#12536=DIRECTION('center_axis',(0.,0.,1.));
#12537=DIRECTION('ref_axis',(1.,0.,0.));
#12538=DIRECTION('center_axis',(0.,0.,1.));
#12539=DIRECTION('ref_axis',(1.,0.,0.));
#15746=CARTESIAN_POINT('',(0.,0.,0.));
#15747=CARTESIAN_POINT('Origin',(4.,0.,6.8));
#15748=CARTESIAN_POINT('',(3.695,-3.73517273739942E-17,7.6));
#15749=CARTESIAN_POINT('Origin',(4.,0.,7.6));
#15750=CARTESIAN_POINT('',(3.695,-3.73517273739942E-17,6.8));
#15751=CARTESIAN_POINT('',(3.695,-3.73517273739942E-17,6.8));
#15752=CARTESIAN_POINT('Origin',(4.,0.,6.8));
#15753=CARTESIAN_POINT('Origin',(4.,0.,6.8));
#15754=CARTESIAN_POINT('',(3.5,-6.12323399573677E-17,7.6));
#15755=CARTESIAN_POINT('Origin',(4.,0.,7.6));
#15756=CARTESIAN_POINT('',(3.5,-6.12323399573677E-17,6.8));
#15757=CARTESIAN_POINT('',(3.5,-6.12323399573677E-17,6.8));
#15758=CARTESIAN_POINT('Origin',(4.,0.,6.8));
#15759=CARTESIAN_POINT('Origin',(4.,0.,7.6));
#15760=CARTESIAN_POINT('Origin',(4.,0.,6.8));
#16592=UNCERTAINTY_MEASURE_WITH_UNIT(LENGTH_MEASURE(0.001),#16679,
'DISTANCE_ACCURACY_VALUE',
'Maximum model space distance between geometric entities at asserted c
onnectivities');
#16614=UNCERTAINTY_MEASURE_WITH_UNIT(LENGTH_MEASURE(0.001),#16679,
'DISTANCE_ACCURACY_VALUE',
'Maximum model space distance between geometric entities at asserted c
onnectivities');
#16656=(
GEOMETRIC_REPRESENTATION_CONTEXT(3)
GLOBAL_UNCERTAINTY_ASSIGNED_CONTEXT((#16592))
GLOBAL_UNIT_ASSIGNED_CONTEXT((#16679,#16681,#16682))
REPRESENTATION_CONTEXT('','3D')
);
#16678=(
GEOMETRIC_REPRESENTATION_CONTEXT(3)
GLOBAL_UNCERTAINTY_ASSIGNED_CONTEXT((#16614))
GLOBAL_UNIT_ASSIGNED_CONTEXT((#16679,#16681,#16682))
REPRESENTATION_CONTEXT('','3D')
);
#16679=(
LENGTH_UNIT()
NAMED_UNIT(*)
SI_UNIT(.CENTI.,.METRE.)
);
#16681=(
NAMED_UNIT(*)
PLANE_ANGLE_UNIT()
SI_UNIT($,.RADIAN.)
);
#16682=(
NAMED_UNIT(*)
SI_UNIT($,.STERADIAN.)
SOLID_ANGLE_UNIT()
);
#16724=SHAPE_DEFINITION_REPRESENTATION(#16795,#16951);
#16795=PRODUCT_DEFINITION_SHAPE('',$,#17015);
#16951=SHAPE_REPRESENTATION('',(#10213),#16656);
#16973=PRODUCT_DEFINITION_CONTEXT('part definition',#17164,'design');
#17015=PRODUCT_DEFINITION('Plain link bushing (2)',
'Plain link bushing (2)',#17078,#16973);
#17078=PRODUCT_DEFINITION_FORMATION('',$,#17207);
#17164=APPLICATION_CONTEXT(
'Core Data for Automotive Mechanical Design Process');
#17165=PRODUCT_CONTEXT('part definition',#17164,'mechanical');
#17207=PRODUCT('Plain link bushing (2)','Plain link bushing (2)',
'Plain link bushing (2)',(#17165));
#17278=COLOUR_RGB('Sky Blue',0.24,0.69,0.87);
#17279=FILL_AREA_STYLE_COLOUR('',#17278);
#17280=FILL_AREA_STYLE('',(#17279));
#17281=SURFACE_STYLE_FILL_AREA(#17280);
#17282=SURFACE_SIDE_STYLE('',(#17281));
#17283=SURFACE_STYLE_USAGE(.BOTH.,#17282);
#17284=PRESENTATION_STYLE_ASSIGNMENT((#17283));
ENDSEC;
END-ISO-10303-21;
